ISO-10303-21;
HEADER;
/* Generated by software containing ST-Developer
 * from STEP Tools, Inc. (www.steptools.com) 
 */

FILE_DESCRIPTION(
/* description */ ('STEP AP214'),
/* implementation_level */ '2;1');

FILE_NAME(
/* name */ 'Plain Washer DIN 125 A 17.step',
/* time_stamp */ '2026-11-14T07:13:32-08:00',
/* author */ (''),
/* organization */ (''),
/* preprocessor_version */ 'ST-DEVELOPER v20.2',
/* originating_system */ 'Autodesk Translation Framework v15.17.0.0',
/* authorisation */ '');

FILE_SCHEMA (('AUTOMOTIVE_DESIGN { 1 0 10303 214 3 1 1 }'));
ENDSEC;

DATA;
#10=MECHANICAL_DESIGN_GEOMETRIC_PRESENTATION_REPRESENTATION('',(#1378),#32903);
#684=SHAPE_REPRESENTATION_RELATIONSHIP('SRR','None',#33026,#698);
#698=ADVANCED_BREP_SHAPE_REPRESENTATION('',(#1467),#32901);
#1058=CIRCLE('',#17054,15.);
#1059=CIRCLE('',#17055,15.);
#1060=CIRCLE('',#17057,8.49999999999999);
#1061=CIRCLE('',#17058,8.49999999999999);
#1287=CYLINDRICAL_SURFACE('',#17053,15.);
#1288=CYLINDRICAL_SURFACE('',#17056,8.49999999999999);
#1378=STYLED_ITEM('',(#33099),#1467);
#1467=MANIFOLD_SOLID_BREP('Body1',#15626);
#1672=FACE_BOUND('',#3644,.T.);
#1673=FACE_BOUND('',#3646,.T.);
#2543=FACE_OUTER_BOUND('',#3641,.T.);
#2544=FACE_OUTER_BOUND('',#3642,.T.);
#2545=FACE_OUTER_BOUND('',#3643,.T.);
#2546=FACE_OUTER_BOUND('',#3645,.T.);
#3641=EDGE_LOOP('',(#13929,#13930,#13931,#13932));
#3642=EDGE_LOOP('',(#13933,#13934,#13935,#13936));
#3643=EDGE_LOOP('',(#13937));
#3644=EDGE_LOOP('',(#13938));
#3645=EDGE_LOOP('',(#13939));
#3646=EDGE_LOOP('',(#13940));
#5065=LINE('',#32651,#6469);
#5066=LINE('',#32657,#6470);
#6469=VECTOR('',#21093,15.);
#6470=VECTOR('',#21100,8.49999999999999);
#7802=VERTEX_POINT('',#32648);
#7803=VERTEX_POINT('',#32650);
#7804=VERTEX_POINT('',#32654);
#7805=VERTEX_POINT('',#32656);
#9848=EDGE_CURVE('',#7802,#7802,#1058,.T.);
#9849=EDGE_CURVE('',#7802,#7803,#5065,.T.);
#9850=EDGE_CURVE('',#7803,#7803,#1059,.T.);
#9851=EDGE_CURVE('',#7804,#7804,#1060,.T.);
#9852=EDGE_CURVE('',#7804,#7805,#5066,.T.);
#9853=EDGE_CURVE('',#7805,#7805,#1061,.T.);
#13929=ORIENTED_EDGE('',*,*,#9848,.F.);
#13930=ORIENTED_EDGE('',*,*,#9849,.T.);
#13931=ORIENTED_EDGE('',*,*,#9850,.T.);
#13932=ORIENTED_EDGE('',*,*,#9849,.F.);
#13933=ORIENTED_EDGE('',*,*,#9851,.F.);
#13934=ORIENTED_EDGE('',*,*,#9852,.T.);
#13935=ORIENTED_EDGE('',*,*,#9853,.T.);
#13936=ORIENTED_EDGE('',*,*,#9852,.F.);
#13937=ORIENTED_EDGE('',*,*,#9850,.F.);
#13938=ORIENTED_EDGE('',*,*,#9851,.T.);
#13939=ORIENTED_EDGE('',*,*,#9848,.T.);
#13940=ORIENTED_EDGE('',*,*,#9853,.F.);
#14634=PLANE('',#17059);
#14635=PLANE('',#17060);
#15511=ADVANCED_FACE('',(#2543),#1287,.T.);
#15512=ADVANCED_FACE('',(#2544),#1288,.F.);
#15513=ADVANCED_FACE('',(#2545,#1672),#14634,.F.);
#15514=ADVANCED_FACE('',(#2546,#1673),#14635,.F.);
#15626=CLOSED_SHELL('',(#15511,#15512,#15513,#15514));
#17052=AXIS2_PLACEMENT_3D('',#32646,#21087,#21088);
#17053=AXIS2_PLACEMENT_3D('',#32647,#21089,#21090);
#17054=AXIS2_PLACEMENT_3D('',#32649,#21091,#21092);
#17055=AXIS2_PLACEMENT_3D('',#32652,#21094,#21095);
#17056=AXIS2_PLACEMENT_3D('',#32653,#21096,#21097);
#17057=AXIS2_PLACEMENT_3D('',#32655,#21098,#21099);
#17058=AXIS2_PLACEMENT_3D('',#32658,#21101,#21102);
#17059=AXIS2_PLACEMENT_3D('',#32659,#21103,#21104);
#17060=AXIS2_PLACEMENT_3D('',#32660,#21105,#21106);
#21087=DIRECTION('axis',(0.,0.,1.));
#21088=DIRECTION('refdir',(1.,0.,0.));
#21089=DIRECTION('center_axis',(-1.,0.,0.));
#21090=DIRECTION('ref_axis',(0.,0.,1.));
#21091=DIRECTION('center_axis',(-1.,0.,0.));
#21092=DIRECTION('ref_axis',(0.,0.,1.));
#21093=DIRECTION('',(1.,0.,0.));
#21094=DIRECTION('center_axis',(-1.,0.,0.));
#21095=DIRECTION('ref_axis',(0.,0.,1.));
#21096=DIRECTION('center_axis',(-1.,0.,0.));
#21097=DIRECTION('ref_axis',(0.,0.,1.));
#21098=DIRECTION('center_axis',(-1.,0.,0.));
#21099=DIRECTION('ref_axis',(0.,0.,1.));
#21100=DIRECTION('',(-1.,0.,0.));
#21101=DIRECTION('center_axis',(-1.,0.,0.));
#21102=DIRECTION('ref_axis',(0.,0.,1.));
#21103=DIRECTION('center_axis',(-1.,0.,0.));
#21104=DIRECTION('ref_axis',(0.,0.,1.));
#21105=DIRECTION('center_axis',(1.,0.,0.));
#21106=DIRECTION('ref_axis',(0.,0.,-1.));
#32646=CARTESIAN_POINT('',(0.,0.,0.));
#32647=CARTESIAN_POINT('Origin',(-34.9249999999999,0.,0.));
#32648=CARTESIAN_POINT('',(-2.99999999999999,-1.83697019872103E-15,-15.));
#32649=CARTESIAN_POINT('Origin',(-3.,0.,0.));
#32650=CARTESIAN_POINT('',(4.44089209850063E-15,-1.83697019872103E-15,-15.));
#32651=CARTESIAN_POINT('',(-34.9249999999999,-1.83697019872103E-15,-15.));
#32652=CARTESIAN_POINT('Origin',(0.,0.,0.));
#32653=CARTESIAN_POINT('Origin',(-34.9249999999999,0.,0.));
#32654=CARTESIAN_POINT('',(-4.44089209850063E-15,-1.04094977927525E-15,
-8.49999999999999));
#32655=CARTESIAN_POINT('Origin',(0.,0.,0.));
#32656=CARTESIAN_POINT('',(-2.99999999999999,-1.04094977927525E-15,-8.49999999999999));
#32657=CARTESIAN_POINT('',(-34.9249999999999,-1.04094977927525E-15,-8.49999999999999));
#32658=CARTESIAN_POINT('Origin',(-3.,0.,0.));
#32659=CARTESIAN_POINT('Origin',(0.,8.49999999999999,0.));
#32660=CARTESIAN_POINT('Origin',(-3.,15.,0.));
#32884=UNCERTAINTY_MEASURE_WITH_UNIT(LENGTH_MEASURE(0.01),#32904,
'DISTANCE_ACCURACY_VALUE',
'Maximum model space distance between geometric entities at asserted c
onnectivities');
#32886=UNCERTAINTY_MEASURE_WITH_UNIT(LENGTH_MEASURE(0.01),#32904,
'DISTANCE_ACCURACY_VALUE',
'Maximum model space distance between geometric entities at asserted c
onnectivities');
#32901=(
GEOMETRIC_REPRESENTATION_CONTEXT(3)
GLOBAL_UNCERTAINTY_ASSIGNED_CONTEXT((#32884))
GLOBAL_UNIT_ASSIGNED_CONTEXT((#32904,#32906,#32907))
REPRESENTATION_CONTEXT('','3D')
);
#32903=(
GEOMETRIC_REPRESENTATION_CONTEXT(3)
GLOBAL_UNCERTAINTY_ASSIGNED_CONTEXT((#32886))
GLOBAL_UNIT_ASSIGNED_CONTEXT((#32904,#32906,#32907))
REPRESENTATION_CONTEXT('','3D')
);
#32904=(
LENGTH_UNIT()
NAMED_UNIT(*)
SI_UNIT(.MILLI.,.METRE.)
);
#32906=(
NAMED_UNIT(*)
PLANE_ANGLE_UNIT()
SI_UNIT($,.RADIAN.)
);
#32907=(
NAMED_UNIT(*)
SI_UNIT($,.STERADIAN.)
SOLID_ANGLE_UNIT()
);
#32922=SHAPE_DEFINITION_REPRESENTATION(#32958,#33026);
#32958=PRODUCT_DEFINITION_SHAPE('',$,#33043);
#33026=SHAPE_REPRESENTATION('',(#17052),#32901);
#33028=PRODUCT_DEFINITION_CONTEXT('part definition',#33078,'design');
#33043=PRODUCT_DEFINITION('Plain Washer DIN 125 A 17',
'Plain Washer DIN 125 A 17',#33059,#33028);
#33059=PRODUCT_DEFINITION_FORMATION('',$,#33094);
#33078=APPLICATION_CONTEXT(
'Core Data for Automotive Mechanical Design Process');
#33079=PRODUCT_CONTEXT('part definition',#33078,'mechanical');
#33094=PRODUCT('Plain Washer DIN 125 A 17','Plain Washer DIN 125 A 17',
$,(#33079));
#33099=PRESENTATION_STYLE_ASSIGNMENT((#33105));
#33105=SURFACE_STYLE_USAGE(.BOTH.,#33111);
#33111=SURFACE_SIDE_STYLE('',(#33117));
#33117=SURFACE_STYLE_FILL_AREA(#33123);
#33123=FILL_AREA_STYLE('Opaque(31,36,43)',(#33129));
#33129=FILL_AREA_STYLE_COLOUR('Opaque(31,36,43)',#33135);
#33135=COLOUR_RGB('Opaque(31,36,43)',0.12156862745098,0.141176470588235,
0.168627450980392);
ENDSEC;
END-ISO-10303-21;
